ISO-10303-21;
HEADER;
FILE_DESCRIPTION (('STEP AP214'),
    '1' );
FILE_NAME ('Lag Sleeve.step',
    '2026-10-22T18:53:08',
    ( '' ),
    ( '' ),
    'SwSTEP 2.0',
    'SolidWorks 2025',
    '' );
FILE_SCHEMA (( 'AUTOMOTIVE_DESIGN' ));
ENDSEC;

DATA;
#19=( LENGTH_UNIT ( ) NAMED_UNIT ( * ) SI_UNIT ( .MILLI., .METRE. ) );
#25=VERTEX_POINT ( 'NONE', #15375 ) ;
#90=ORIENTED_EDGE ( 'NONE', *, *, #11501, .F. ) ;
#147=CARTESIAN_POINT ( 'NONE',  ( -10.83999999999999986, -14.99147757894464306, 15.50000000000000000 ) ) ;
#160=FACE_OUTER_BOUND ( 'NONE', #18742, .T. ) ;
#243=EDGE_LOOP ( 'NONE', ( #6237, #14444, #13693, #2734 ) ) ;
#245=ADVANCED_FACE ( 'NONE', ( #4620, #9951 ), #15830, .F. ) ;
#390=CARTESIAN_POINT ( 'NONE',  ( 0.000000000000000000, -14.99147757894464306, 7.750000000000000000 ) ) ;
#398=EDGE_CURVE ( 'NONE', #9329, #12017, #10900, .T. ) ;
#434=AXIS2_PLACEMENT_3D ( 'NONE', #1812, #20123, #9338 ) ;
#439=CARTESIAN_POINT ( 'NONE',  ( 0.000000000000000000, 0.000000000000000000, 0.000000000000000000 ) ) ;
#560=ADVANCED_FACE ( 'NONE', ( #19147 ), #6469, .F. ) ;
#603=ADVANCED_FACE ( 'NONE', ( #24066 ), #23395, .F. ) ;
#604=LINE ( 'NONE', #20609, #11879 ) ;
#607=CARTESIAN_POINT ( 'NONE',  ( 18.50000000000000000, 2.265596578422603396E-15, 15.50000000000000000 ) ) ;
#608=CARTESIAN_POINT ( 'NONE',  ( -18.50000000000000000, 0.000000000000000000, 0.000000000000000000 ) ) ;
#625=LINE ( 'NONE', #9500, #16822 ) ;
#771=ORIENTED_EDGE ( 'NONE', *, *, #9688, .T. ) ;
#777=AXIS2_PLACEMENT_3D ( 'NONE', #5867, #22960, #13295 ) ;
#893=CIRCLE ( 'NONE', #14139, 9.999999999999998224 ) ;
#946=ORIENTED_EDGE ( 'NONE', *, *, #19577, .F. ) ;
#1287=CIRCLE ( 'NONE', #10595, 0.9999999999999991118 ) ;
#1428=DIRECTION ( 'NONE',  ( -0.000000000000000000, -0.000000000000000000, -1.000000000000000000 ) ) ;
#1467=CARTESIAN_POINT ( 'NONE',  ( 0.000000000000000000, 0.000000000000000000, 0.000000000000000000 ) ) ;
#1489=CARTESIAN_POINT ( 'NONE',  ( 0.000000000000000000, 0.000000000000000000, 15.50000000000000000 ) ) ;
#1517=CARTESIAN_POINT ( 'NONE',  ( 0.000000000000000000, -12.99147757894464306, 7.750000000000000000 ) ) ;
#1534=CYLINDRICAL_SURFACE ( 'NONE', #19218, 18.50000000000000000 ) ;
#1536=EDGE_CURVE ( 'NONE', #13092, #7965, #20749, .T. ) ;
#1548=ORIENTED_EDGE ( 'NONE', *, *, #18401, .F. ) ;
#1577=AXIS2_PLACEMENT_3D ( 'NONE', #9140, #24039, #14752 ) ;
#1750=VECTOR ( 'NONE', #2488, 1000.000000000000000 ) ;
#1769=CYLINDRICAL_SURFACE ( 'NONE', #23841, 9.999999999999998224 ) ;
#1787=DIRECTION ( 'NONE',  ( 0.000000000000000000, 0.000000000000000000, -1.000000000000000000 ) ) ;
#1812=CARTESIAN_POINT ( 'NONE',  ( 0.000000000000000000, 0.000000000000000000, 0.000000000000000000 ) ) ;
#1831=DIRECTION ( 'NONE',  ( 1.000000000000000000, 0.000000000000000000, -0.000000000000000000 ) ) ;
#1868=DIRECTION ( 'NONE',  ( 0.000000000000000000, 0.000000000000000000, -1.000000000000000000 ) ) ;
#1910=CARTESIAN_POINT ( 'NONE',  ( -18.50000000000000000, 0.000000000000000000, 15.50000000000000000 ) ) ;
#1973=PRODUCT ( 'Lag Sleeve', 'Lag Sleeve', '', ( #13112 ) ) ;
#2036=VERTEX_POINT ( 'NONE', #3685 ) ;
#2057=SHAPE_REPRESENTATION ( 'Lag Sleeve', ( #8005 ), #21672 ) ;
#2221=CARTESIAN_POINT ( 'NONE',  ( 0.000000000000000000, -14.99147757894464306, 7.750000000000000000 ) ) ;
#2223=DIRECTION ( 'NONE',  ( 0.000000000000000000, 0.000000000000000000, 1.000000000000000000 ) ) ;
#2332=CYLINDRICAL_SURFACE ( 'NONE', #777, 18.50000000000000000 ) ;
#2367=EDGE_CURVE ( 'NONE', #14658, #9329, #8359, .T. ) ;
#2397=VECTOR ( 'NONE', #20885, 1000.000000000000000 ) ;
#2488=DIRECTION ( 'NONE',  ( -0.000000000000000000, -1.000000000000000000, -0.000000000000000000 ) ) ;
#2599=PRODUCT_DEFINITION ( 'UNKNOWN', '', #19357, #19203 ) ;
#2629=EDGE_CURVE ( 'NONE', #14658, #25, #12091, .T. ) ;
#2726=ORIENTED_EDGE ( 'NONE', *, *, #9425, .T. ) ;
#2734=ORIENTED_EDGE ( 'NONE', *, *, #10546, .F. ) ;
#2793=STYLED_ITEM('',(#24141),#10843);
#2806=PRODUCT_DEFINITION_SHAPE ( 'NONE', 'NONE',  #2599 ) ;
#2817=DIRECTION ( 'NONE',  ( -0.000000000000000000, -1.000000000000000000, -0.000000000000000000 ) ) ;
#2830=ORIENTED_EDGE ( 'NONE', *, *, #9423, .F. ) ;
#2843=AXIS2_PLACEMENT_3D ( 'NONE', #1467, #20121, #16316 ) ;
#2955=CARTESIAN_POINT ( 'NONE',  ( 0.000000000000000000, -12.99147757894464306, 7.750000000000000000 ) ) ;
#3066=CIRCLE ( 'NONE', #14735, 18.50000000000000000 ) ;
#3078=CARTESIAN_POINT ( 'NONE',  ( 10.83999999999999986, -14.99147757894464306, 0.000000000000000000 ) ) ;
#3112=CARTESIAN_POINT ( 'NONE',  ( -9.999999999999998224, 0.000000000000000000, 15.50000000000000000 ) ) ;
#3267=ORIENTED_EDGE ( 'NONE', *, *, #5847, .F. ) ;
#3420=FACE_BOUND ( 'NONE', #7408, .T. ) ;
#3453=VECTOR ( 'NONE', #4865, 1000.000000000000000 ) ;
#3498=DIRECTION ( 'NONE',  ( -0.000000000000000000, -0.000000000000000000, -1.000000000000000000 ) ) ;
#3531=CARTESIAN_POINT ( 'NONE',  ( 0.000000000000000000, 0.000000000000000000, 0.000000000000000000 ) ) ;
#3612=EDGE_CURVE ( 'NONE', #8536, #7965, #3066, .T. ) ;
#3685=CARTESIAN_POINT ( 'NONE',  ( 0.000000000000000000, -12.99147757894464306, 6.750000000000000888 ) ) ;
#3687=VERTEX_POINT ( 'NONE', #7623 ) ;
#3736=CARTESIAN_POINT ( 'NONE',  ( 0.000000000000000000, -14.96647757894464270, 7.750000000000000000 ) ) ;
#3749=EDGE_LOOP ( 'NONE', ( #4895, #9749, #23837 ) ) ;
#3832=CARTESIAN_POINT ( 'NONE',  ( 0.000000000000000000, 0.000000000000000000, 15.50000000000000000 ) ) ;
#3848=SHAPE_DEFINITION_REPRESENTATION ( #2806, #2057 ) ;
#3902=VERTEX_POINT ( 'NONE', #7006 ) ;
#3928=CIRCLE ( 'NONE', #11691, 18.50000000000000000 ) ;
#4007=ORIENTED_EDGE ( 'NONE', *, *, #9250, .T. ) ;
#4056=PLANE ( 'NONE',  #14803 ) ;
#4083=VECTOR ( 'NONE', #4818, 1000.000000000000000 ) ;
#4124=ORIENTED_EDGE ( 'NONE', *, *, #6793, .T. ) ;
#4242=EDGE_LOOP ( 'NONE', ( #18336, #20675, #7375, #13202 ) ) ;
#4253=LINE ( 'NONE', #5834, #20104 ) ;
#4269=ORIENTED_EDGE ( 'NONE', *, *, #18401, .T. ) ;
#4333=ORIENTED_EDGE ( 'NONE', *, *, #12912, .F. ) ;
#4496=CIRCLE ( 'NONE', #6042, 0.9999999999999991118 ) ;
#4499=ORIENTED_EDGE ( 'NONE', *, *, #398, .F. ) ;
#4605=LINE ( 'NONE', #23276, #12956 ) ;
#4620=FACE_BOUND ( 'NONE', #9342, .T. ) ;
#4703=VERTEX_POINT ( 'NONE', #4798 ) ;
#4749=LINE ( 'NONE', #23659, #18427 ) ;
#4753=ORIENTED_EDGE ( 'NONE', *, *, #2367, .F. ) ;
#4778=VERTEX_POINT ( 'NONE', #3078 ) ;
#4798=CARTESIAN_POINT ( 'NONE',  ( 0.000000000000000000, -14.96647757894464270, 6.750000000000000888 ) ) ;
#4818=DIRECTION ( 'NONE',  ( -0.000000000000000000, -0.000000000000000000, -1.000000000000000000 ) ) ;
#4865=DIRECTION ( 'NONE',  ( -0.000000000000000000, -0.000000000000000000, -1.000000000000000000 ) ) ;
#4881=DIRECTION ( 'NONE',  ( 1.000000000000000000, 0.000000000000000000, 0.000000000000000000 ) ) ;
#4895=ORIENTED_EDGE ( 'NONE', *, *, #9250, .F. ) ;
#5000=CARTESIAN_POINT ( 'NONE',  ( 0.000000000000000000, 0.000000000000000000, 15.50000000000000000 ) ) ;
#5063=ADVANCED_FACE ( 'NONE', ( #8793 ), #6010, .F. ) ;
#5432=DIRECTION ( 'NONE',  ( 0.000000000000000000, -0.7071067811865536790, -0.7071067811865414665 ) ) ;
#5439=AXIS2_PLACEMENT_3D ( 'NONE', #8106, #15550, #8361 ) ;
#5468=VERTEX_POINT ( 'NONE', #7596 ) ;
#5472=EDGE_CURVE ( 'NONE', #7070, #16945, #17004, .T. ) ;
#5511=DIRECTION ( 'NONE',  ( -0.000000000000000000, -1.000000000000000000, -0.000000000000000000 ) ) ;
#5547=VERTEX_POINT ( 'NONE', #11867 ) ;
#5643=ORIENTED_EDGE ( 'NONE', *, *, #5472, .T. ) ;
#5731=ORIENTED_EDGE ( 'NONE', *, *, #18298, .F. ) ;
#5809=DIRECTION ( 'NONE',  ( 0.000000000000000000, 0.000000000000000000, 1.000000000000000000 ) ) ;
#5814=( NAMED_UNIT ( * ) PLANE_ANGLE_UNIT ( ) SI_UNIT ( $, .RADIAN. ) );
#5834=CARTESIAN_POINT ( 'NONE',  ( 10.83999999999999986, -14.99147757894464306, 15.50000000000000000 ) ) ;
#5847=EDGE_CURVE ( 'NONE', #8138, #12085, #17663, .T. ) ;
#5867=CARTESIAN_POINT ( 'NONE',  ( 0.000000000000000000, 0.000000000000000000, 15.50000000000000000 ) ) ;
#5978=CARTESIAN_POINT ( 'NONE',  ( 0.000000000000000000, 0.000000000000000000, 0.000000000000000000 ) ) ;
#5996=VECTOR ( 'NONE', #5432, 1000.000000000000000 ) ;
#6010=CONICAL_SURFACE ( 'NONE', #20847, 0.9999999999999991118, 1.029744258676654090 ) ;
#6042=AXIS2_PLACEMENT_3D ( 'NONE', #3736, #10797, #1787 ) ;
#6094=DIRECTION ( 'NONE',  ( 0.000000000000000000, 0.000000000000000000, 1.000000000000000000 ) ) ;
#6122=CYLINDRICAL_SURFACE ( 'NONE', #21184, 0.9999999999999991118 ) ;
#6125=ORIENTED_EDGE ( 'NONE', *, *, #21199, .F. ) ;
#6196=DIRECTION ( 'NONE',  ( 0.000000000000000000, 0.000000000000000000, 1.000000000000000000 ) ) ;
#6209=DIRECTION ( 'NONE',  ( 1.000000000000000000, 0.000000000000000000, 0.000000000000000000 ) ) ;
#6237=ORIENTED_EDGE ( 'NONE', *, *, #6793, .F. ) ;
#6247=ORIENTED_EDGE ( 'NONE', *, *, #22139, .T. ) ;
#6445=DIRECTION ( 'NONE',  ( 0.000000000000000000, 1.000000000000000000, 0.000000000000000000 ) ) ;
#6469=CYLINDRICAL_SURFACE ( 'NONE', #18310, 9.999999999999998224 ) ;
#6484=CIRCLE ( 'NONE', #13095, 18.50000000000000000 ) ;
#6569=CARTESIAN_POINT ( 'NONE',  ( 0.000000000000000000, 0.000000000000000000, 15.50000000000000000 ) ) ;
#6768=ORIENTED_EDGE ( 'NONE', *, *, #19577, .T. ) ;
#6771=AXIS2_PLACEMENT_3D ( 'NONE', #2221, #5511, #14892 ) ;
#6793=EDGE_CURVE ( 'NONE', #4778, #5547, #9814, .T. ) ;
#7002=EDGE_LOOP ( 'NONE', ( #1548, #19884, #20583, #9816 ) ) ;
#7006=CARTESIAN_POINT ( 'NONE',  ( 10.83999999999999986, -14.99147757894464306, 15.50000000000000000 ) ) ;
#7056=EDGE_CURVE ( 'NONE', #7965, #4778, #11248, .T. ) ;
#7070=VERTEX_POINT ( 'NONE', #14805 ) ;
#7195=FACE_OUTER_BOUND ( 'NONE', #19456, .T. ) ;
#7256=FACE_OUTER_BOUND ( 'NONE', #10322, .T. ) ;
#7353=CLOSED_SHELL ( 'NONE', ( #603, #12731, #5063, #560, #20519, #19760, #17951, #18884, #7975, #245, #11020, #20683, #20110, #13869 ) ) ;
#7375=ORIENTED_EDGE ( 'NONE', *, *, #9688, .F. ) ;
#7404=EDGE_CURVE ( 'NONE', #7070, #2036, #1287, .T. ) ;
#7408=EDGE_LOOP ( 'NONE', ( #16048, #11106 ) ) ;
#7458=CIRCLE ( 'NONE', #21121, 0.9999999999999991118 ) ;
#7596=CARTESIAN_POINT ( 'NONE',  ( -6.370271264241011523E-16, -12.39061695991708412, 7.750000000000000000 ) ) ;
#7623=CARTESIAN_POINT ( 'NONE',  ( 18.50000000000000000, 2.265596578422603396E-15, 15.50000000000000000 ) ) ;
#7797=DIRECTION ( 'NONE',  ( 0.000000000000000000, 0.000000000000000000, -1.000000000000000000 ) ) ;
#7801=FACE_OUTER_BOUND ( 'NONE', #21153, .T. ) ;
#7965=VERTEX_POINT ( 'NONE', #10311 ) ;
#7975=ADVANCED_FACE ( 'NONE', ( #14326 ), #1534, .T. ) ;
#7977=EDGE_LOOP ( 'NONE', ( #4753, #8032 ) ) ;
#8005=AXIS2_PLACEMENT_3D ( 'NONE', #5978, #22344, #13412 ) ;
#8032=ORIENTED_EDGE ( 'NONE', *, *, #8564, .F. ) ;
#8106=CARTESIAN_POINT ( 'NONE',  ( 0.000000000000000000, -14.99147757894464306, 7.750000000000000000 ) ) ;
#8138=VERTEX_POINT ( 'NONE', #19795 ) ;
#8298=DIRECTION ( 'NONE',  ( 0.000000000000000000, 0.000000000000000000, -1.000000000000000000 ) ) ;
#8310=EDGE_LOOP ( 'NONE', ( #21477, #9802, #5731, #10382 ) ) ;
#8359=CIRCLE ( 'NONE', #11450, 9.999999999999998224 ) ;
#8361=DIRECTION ( 'NONE',  ( 0.000000000000000000, 0.000000000000000000, -1.000000000000000000 ) ) ;
#8513=CARTESIAN_POINT ( 'NONE',  ( 0.000000000000000000, -12.99147757894464306, 7.750000000000000000 ) ) ;
#8536=VERTEX_POINT ( 'NONE', #608 ) ;
#8564=EDGE_CURVE ( 'NONE', #9329, #14658, #12136, .T. ) ;
#8616=DIRECTION ( 'NONE',  ( 1.049727191138618449E-16, -0.5150380749100544886, 0.8571673007021121116 ) ) ;
#8662=AXIS2_PLACEMENT_3D ( 'NONE', #12159, #19985, #4881 ) ;
#8793=FACE_OUTER_BOUND ( 'NONE', #18505, .T. ) ;
#8939=CARTESIAN_POINT ( 'NONE',  ( 1.255262969126036846E-16, -14.99147757894464306, 8.775000000000000355 ) ) ;
#8953=LINE ( 'NONE', #23749, #5996 ) ;
#9004=ORIENTED_EDGE ( 'NONE', *, *, #12912, .T. ) ;
#9100=LINE ( 'NONE', #1910, #14883 ) ;
#9109=AXIS2_PLACEMENT_3D ( 'NONE', #16208, #21939, #20232 ) ;
#9140=CARTESIAN_POINT ( 'NONE',  ( 0.000000000000000000, -14.99147757894464306, 7.750000000000000000 ) ) ;
#9142=EDGE_CURVE ( 'NONE', #2036, #7070, #7458, .T. ) ;
#9219=DIRECTION ( 'NONE',  ( 0.000000000000000000, -0.5150380749100544886, -0.8571673007021121116 ) ) ;
#9250=EDGE_CURVE ( 'NONE', #5468, #7070, #4749, .T. ) ;
#9329=VERTEX_POINT ( 'NONE', #14240 ) ;
#9338=DIRECTION ( 'NONE',  ( 1.000000000000000000, 0.000000000000000000, 0.000000000000000000 ) ) ;
#9342=EDGE_LOOP ( 'NONE', ( #3267, #946 ) ) ;
#9353=CIRCLE ( 'NONE', #434, 9.999999999999998224 ) ;
#9384=ORIENTED_EDGE ( 'NONE', *, *, #7404, .T. ) ;
#9423=EDGE_CURVE ( 'NONE', #12017, #25, #893, .T. ) ;
#9425=EDGE_CURVE ( 'NONE', #15969, #8536, #9100, .T. ) ;
#9436=ORIENTED_EDGE ( 'NONE', *, *, #17295, .T. ) ;
#9500=CARTESIAN_POINT ( 'NONE',  ( 0.000000000000000000, -14.99147757894464306, 6.750000000000000888 ) ) ;
#9584=( NAMED_UNIT ( * ) SI_UNIT ( $, .STERADIAN. ) SOLID_ANGLE_UNIT ( ) );
#9614=ORIENTED_EDGE ( 'NONE', *, *, #21199, .T. ) ;
#9688=EDGE_CURVE ( 'NONE', #13092, #3902, #4605, .T. ) ;
#9709=AXIS2_PLACEMENT_3D ( 'NONE', #22936, #6094, #6209 ) ;
#9749=ORIENTED_EDGE ( 'NONE', *, *, #16187, .T. ) ;
#9802=ORIENTED_EDGE ( 'NONE', *, *, #398, .T. ) ;
#9814=CIRCLE ( 'NONE', #2843, 18.50000000000000000 ) ;
#9816=ORIENTED_EDGE ( 'NONE', *, *, #9425, .F. ) ;
#9951=FACE_OUTER_BOUND ( 'NONE', #4242, .T. ) ;
#10083=DIRECTION ( 'NONE',  ( 0.000000000000000000, 0.000000000000000000, -1.000000000000000000 ) ) ;
#10114=ORIENTED_EDGE ( 'NONE', *, *, #5847, .T. ) ;
#10311=CARTESIAN_POINT ( 'NONE',  ( -10.83999999999999986, -14.99147757894464306, 0.000000000000000000 ) ) ;
#10322=EDGE_LOOP ( 'NONE', ( #4499, #20435, #19554, #2830 ) ) ;
#10366=EDGE_CURVE ( 'NONE', #3687, #5547, #18903, .T. ) ;
#10382=ORIENTED_EDGE ( 'NONE', *, *, #2629, .F. ) ;
#10494=DIRECTION ( 'NONE',  ( 0.000000000000000000, 0.000000000000000000, -1.000000000000000000 ) ) ;
#10546=EDGE_CURVE ( 'NONE', #5547, #8536, #21539, .T. ) ;
#10595=AXIS2_PLACEMENT_3D ( 'NONE', #1517, #12470, #19710 ) ;
#10797=DIRECTION ( 'NONE',  ( -0.000000000000000000, -1.000000000000000000, -0.000000000000000000 ) ) ;
#10810=DIRECTION ( 'NONE',  ( 1.000000000000000000, 0.000000000000000000, 0.000000000000000000 ) ) ;
#10843=MANIFOLD_SOLID_BREP ( '\X2\00d8\X0\2.0mm Dowel Hole1', #7353 ) ;
#10900=LINE ( 'NONE', #18367, #3453 ) ;
#10911=CARTESIAN_POINT ( 'NONE',  ( 0.000000000000000000, 0.000000000000000000, 0.000000000000000000 ) ) ;
#10916=DIRECTION ( 'NONE',  ( 0.000000000000000000, 0.000000000000000000, 1.000000000000000000 ) ) ;
#10947=DIRECTION ( 'NONE',  ( 0.000000000000000000, 0.000000000000000000, 1.000000000000000000 ) ) ;
#11020=ADVANCED_FACE ( 'NONE', ( #7256 ), #1769, .F. ) ;
#11106=ORIENTED_EDGE ( 'NONE', *, *, #9423, .T. ) ;
#11248=LINE ( 'NONE', #20432, #18056 ) ;
#11260=CARTESIAN_POINT ( 'NONE',  ( 0.000000000000000000, -12.99147757894464306, 6.750000000000000888 ) ) ;
#11329=CARTESIAN_POINT ( 'NONE',  ( 0.000000000000000000, 0.000000000000000000, 15.50000000000000000 ) ) ;
#11450=AXIS2_PLACEMENT_3D ( 'NONE', #1489, #10947, #20495 ) ;
#11501=EDGE_CURVE ( 'NONE', #2036, #4703, #625, .T. ) ;
#11577=DIRECTION ( 'NONE',  ( -0.000000000000000000, -1.000000000000000000, -0.000000000000000000 ) ) ;
#11691=AXIS2_PLACEMENT_3D ( 'NONE', #23512, #19853, #16047 ) ;
#11804=DIRECTION ( 'NONE',  ( -1.000000000000000000, 0.000000000000000000, 0.000000000000000000 ) ) ;
#11867=CARTESIAN_POINT ( 'NONE',  ( 18.50000000000000000, 2.265596578422603396E-15, 0.000000000000000000 ) ) ;
#11879=VECTOR ( 'NONE', #15466, 1000.000000000000000 ) ;
#12017=VERTEX_POINT ( 'NONE', #22555 ) ;
#12085=VERTEX_POINT ( 'NONE', #8939 ) ;
#12091=LINE ( 'NONE', #23472, #4083 ) ;
#12136=CIRCLE ( 'NONE', #13367, 9.999999999999998224 ) ;
#12155=DIRECTION ( 'NONE',  ( -0.000000000000000000, -1.000000000000000000, -0.000000000000000000 ) ) ;
#12159=CARTESIAN_POINT ( 'NONE',  ( 0.000000000000000000, 0.000000000000000000, 0.000000000000000000 ) ) ;
#12201=CARTESIAN_POINT ( 'NONE',  ( 0.000000000000000000, -14.96647757894464270, 7.750000000000000000 ) ) ;
#12349=ORIENTED_EDGE ( 'NONE', *, *, #22139, .F. ) ;
#12442=ORIENTED_EDGE ( 'NONE', *, *, #15188, .F. ) ;
#12470=DIRECTION ( 'NONE',  ( -0.000000000000000000, -1.000000000000000000, -0.000000000000000000 ) ) ;
#12731=ADVANCED_FACE ( 'NONE', ( #160 ), #6122, .F. ) ;
#12912=EDGE_CURVE ( 'NONE', #4703, #16945, #20091, .T. ) ;
#12953=CARTESIAN_POINT ( 'NONE',  ( 0.000000000000000000, -14.99147757894464306, 7.750000000000000000 ) ) ;
#12956=VECTOR ( 'NONE', #17769, 1000.000000000000000 ) ;
#13047=( NAMED_UNIT ( * ) PLANE_ANGLE_UNIT ( ) SI_UNIT ( $, .RADIAN. ) );
#13092=VERTEX_POINT ( 'NONE', #19799 ) ;
#13095=AXIS2_PLACEMENT_3D ( 'NONE', #6569, #6196, #14003 ) ;
#13112=PRODUCT_CONTEXT ( 'NONE', #21484, 'mechanical' ) ;
#13202=ORIENTED_EDGE ( 'NONE', *, *, #1536, .T. ) ;
#13295=DIRECTION ( 'NONE',  ( -1.000000000000000000, 0.000000000000000000, 0.000000000000000000 ) ) ;
#13335=CARTESIAN_POINT ( 'NONE',  ( 1.224646799147352714E-16, -14.99147757894464306, 8.749999999999998224 ) ) ;
#13367=AXIS2_PLACEMENT_3D ( 'NONE', #5000, #10916, #10810 ) ;
#13412=DIRECTION ( 'NONE',  ( 1.000000000000000000, 0.000000000000000000, 0.000000000000000000 ) ) ;
#13684=AXIS2_PLACEMENT_3D ( 'NONE', #3531, #21841, #1831 ) ;
#13693=ORIENTED_EDGE ( 'NONE', *, *, #3612, .F. ) ;
#13869=ADVANCED_FACE ( 'NONE', ( #23677 ), #16235, .F. ) ;
#13920=DIRECTION ( 'NONE',  ( 0.000000000000000000, 0.000000000000000000, 1.000000000000000000 ) ) ;
#14003=DIRECTION ( 'NONE',  ( 1.000000000000000000, 0.000000000000000000, 0.000000000000000000 ) ) ;
#14066=EDGE_LOOP ( 'NONE', ( #6125, #4333, #9436, #10114 ) ) ;
#14078=MECHANICAL_DESIGN_GEOMETRIC_PRESENTATION_REPRESENTATION('',(#2793),#17175);
#14139=AXIS2_PLACEMENT_3D ( 'NONE', #10911, #13920, #22423 ) ;
#14239=AXIS2_PLACEMENT_3D ( 'NONE', #12201, #2817, #8298 ) ;
#14240=CARTESIAN_POINT ( 'NONE',  ( 9.999999999999998224, 1.224646799147353059E-15, 15.50000000000000000 ) ) ;
#14326=FACE_OUTER_BOUND ( 'NONE', #18163, .T. ) ;
#14444=ORIENTED_EDGE ( 'NONE', *, *, #7056, .F. ) ;
#14613=DIRECTION ( 'NONE',  ( 0.000000000000000000, 0.000000000000000000, -1.000000000000000000 ) ) ;
#14658=VERTEX_POINT ( 'NONE', #3112 ) ;
#14735=AXIS2_PLACEMENT_3D ( 'NONE', #439, #5809, #19108 ) ;
#14752=DIRECTION ( 'NONE',  ( 0.000000000000000000, 0.000000000000000000, -1.000000000000000000 ) ) ;
#14762=SHAPE_REPRESENTATION_RELATIONSHIP ( 'NONE' , 'NONE' ,  #2057, #18057 ) ;
#14803=AXIS2_PLACEMENT_3D ( 'NONE', #11329, #2223, #20403 ) ;
#14805=CARTESIAN_POINT ( 'NONE',  ( 1.224646799147352468E-16, -12.99147757894464306, 8.749999999999998224 ) ) ;
#14853=FACE_OUTER_BOUND ( 'NONE', #243, .T. ) ;
#14883=VECTOR ( 'NONE', #3498, 1000.000000000000000 ) ;
#14892=DIRECTION ( 'NONE',  ( 0.000000000000000000, 0.000000000000000000, -1.000000000000000000 ) ) ;
#14930=VECTOR ( 'NONE', #9219, 1000.000000000000000 ) ;
#14968=CARTESIAN_POINT ( 'NONE',  ( -18.50000000000000000, 0.000000000000000000, 15.50000000000000000 ) ) ;
#15070=( LENGTH_UNIT ( ) NAMED_UNIT ( * ) SI_UNIT ( .MILLI., .METRE. ) );
#15141=EDGE_LOOP ( 'NONE', ( #12442, #9614, #6768, #19503 ) ) ;
#15188=EDGE_CURVE ( 'NONE', #16945, #4703, #4496, .T. ) ;
#15215=( NAMED_UNIT ( * ) SI_UNIT ( $, .STERADIAN. ) SOLID_ANGLE_UNIT ( ) );
#15375=CARTESIAN_POINT ( 'NONE',  ( -9.999999999999998224, 0.000000000000000000, 0.000000000000000000 ) ) ;
#15413=ORIENTED_EDGE ( 'NONE', *, *, #20208, .F. ) ;
#15448=ORIENTED_EDGE ( 'NONE', *, *, #7404, .F. ) ;
#15466=DIRECTION ( 'NONE',  ( 8.659560562354857670E-17, -0.7071067811865536790, 0.7071067811865414665 ) ) ;
#15477=DIRECTION ( 'NONE',  ( -0.000000000000000000, -0.000000000000000000, -1.000000000000000000 ) ) ;
#15550=DIRECTION ( 'NONE',  ( -0.000000000000000000, -1.000000000000000000, -0.000000000000000000 ) ) ;
#15706=CARTESIAN_POINT ( 'NONE',  ( 1.224646799147353207E-16, -14.96647757894464270, 8.749999999999998224 ) ) ;
#15748=ORIENTED_EDGE ( 'NONE', *, *, #1536, .F. ) ;
#15830=PLANE ( 'NONE',  #21433 ) ;
#15969=VERTEX_POINT ( 'NONE', #14968 ) ;
#16047=DIRECTION ( 'NONE',  ( 1.000000000000000000, 0.000000000000000000, 0.000000000000000000 ) ) ;
#16048=ORIENTED_EDGE ( 'NONE', *, *, #18298, .T. ) ;
#16187=EDGE_CURVE ( 'NONE', #5468, #2036, #18625, .T. ) ;
#16208=CARTESIAN_POINT ( 'NONE',  ( 0.000000000000000000, 0.000000000000000000, 15.50000000000000000 ) ) ;
#16235=CONICAL_SURFACE ( 'NONE', #18952, 1.024999999999999911, 0.7853981633974396193 ) ;
#16239=DIRECTION ( 'NONE',  ( -0.000000000000000000, -1.000000000000000000, -0.000000000000000000 ) ) ;
#16274=ORIENTED_EDGE ( 'NONE', *, *, #11501, .T. ) ;
#16316=DIRECTION ( 'NONE',  ( 1.000000000000000000, 0.000000000000000000, 0.000000000000000000 ) ) ;
#16523=DIRECTION ( 'NONE',  ( -0.000000000000000000, -0.000000000000000000, -1.000000000000000000 ) ) ;
#16648=DIRECTION ( 'NONE',  ( -1.000000000000000000, 0.000000000000000000, 0.000000000000000000 ) ) ;
#16822=VECTOR ( 'NONE', #11577, 1000.000000000000000 ) ;
#16945=VERTEX_POINT ( 'NONE', #15706 ) ;
#17004=LINE ( 'NONE', #13335, #1750 ) ;
#17090=FACE_BOUND ( 'NONE', #7977, .T. ) ;
#17135=ORIENTED_EDGE ( 'NONE', *, *, #22969, .T. ) ;
#17168=DIRECTION ( 'NONE',  ( 0.000000000000000000, 0.000000000000000000, -1.000000000000000000 ) ) ;
#17175=( GEOMETRIC_REPRESENTATION_CONTEXT ( 3 ) GLOBAL_UNCERTAINTY_ASSIGNED_CONTEXT ( ( #21335 ) ) GLOBAL_UNIT_ASSIGNED_CONTEXT ( ( #15070, #5814, #9584 ) ) REPRESENTATION_CONTEXT ( 'NONE', 'WORKASPACE' ) );
#17295=EDGE_CURVE ( 'NONE', #4703, #8138, #8953, .T. ) ;
#17297=ORIENTED_EDGE ( 'NONE', *, *, #3612, .T. ) ;
#17539=DIRECTION ( 'NONE',  ( -0.000000000000000000, -0.000000000000000000, -1.000000000000000000 ) ) ;
#17663=CIRCLE ( 'NONE', #6771, 1.024999999999999911 ) ;
#17769=DIRECTION ( 'NONE',  ( 1.000000000000000000, 0.000000000000000000, 0.000000000000000000 ) ) ;
#17951=ADVANCED_FACE ( 'NONE', ( #7801, #17090 ), #4056, .T. ) ;
#18047=DIRECTION ( 'NONE',  ( -0.000000000000000000, -1.000000000000000000, -0.000000000000000000 ) ) ;
#18056=VECTOR ( 'NONE', #22399, 1000.000000000000000 ) ;
#18057=ADVANCED_BREP_SHAPE_REPRESENTATION ( '', ( #10843, #8005 ), #21672 ) ;
#18065=APPLICATION_CONTEXT ( 'automotive_design' ) ;
#18163=EDGE_LOOP ( 'NONE', ( #21472, #12349, #17135, #4124 ) ) ;
#18298=EDGE_CURVE ( 'NONE', #25, #12017, #9353, .T. ) ;
#18310=AXIS2_PLACEMENT_3D ( 'NONE', #21470, #15477, #11804 ) ;
#18315=CIRCLE ( 'NONE', #5439, 1.024999999999999911 ) ;
#18336=ORIENTED_EDGE ( 'NONE', *, *, #7056, .T. ) ;
#18367=CARTESIAN_POINT ( 'NONE',  ( 9.999999999999998224, 1.224646799147353059E-15, 15.50000000000000000 ) ) ;
#18391=CYLINDRICAL_SURFACE ( 'NONE', #9109, 18.50000000000000000 ) ;
#18395=ORIENTED_EDGE ( 'NONE', *, *, #9142, .F. ) ;
#18401=EDGE_CURVE ( 'NONE', #3687, #15969, #3928, .T. ) ;
#18427=VECTOR ( 'NONE', #8616, 1000.000000000000000 ) ;
#18505=EDGE_LOOP ( 'NONE', ( #24071, #4007, #9384 ) ) ;
#18625=LINE ( 'NONE', #11260, #14930 ) ;
#18643=ORIENTED_EDGE ( 'NONE', *, *, #5472, .F. ) ;
#18691=DIRECTION ( 'NONE',  ( -0.000000000000000000, -1.000000000000000000, -0.000000000000000000 ) ) ;
#18742=EDGE_LOOP ( 'NONE', ( #15448, #5643, #23727, #90 ) ) ;
#18884=ADVANCED_FACE ( 'NONE', ( #14853, #3420 ), #20367, .F. ) ;
#18903=LINE ( 'NONE', #607, #23491 ) ;
#18952=AXIS2_PLACEMENT_3D ( 'NONE', #23898, #18047, #14613 ) ;
#19108=DIRECTION ( 'NONE',  ( 1.000000000000000000, 0.000000000000000000, 0.000000000000000000 ) ) ;
#19147=FACE_OUTER_BOUND ( 'NONE', #8310, .T. ) ;
#19203=PRODUCT_DEFINITION_CONTEXT ( 'detailed design', #18065, 'design' ) ;
#19218=AXIS2_PLACEMENT_3D ( 'NONE', #21791, #1428, #23277 ) ;
#19357=PRODUCT_DEFINITION_FORMATION_WITH_SPECIFIED_SOURCE ( 'ANY', '', #1973, .NOT_KNOWN. ) ;
#19456=EDGE_LOOP ( 'NONE', ( #18643, #18395, #16274, #9004 ) ) ;
#19503=ORIENTED_EDGE ( 'NONE', *, *, #17295, .F. ) ;
#19554=ORIENTED_EDGE ( 'NONE', *, *, #2629, .T. ) ;
#19577=EDGE_CURVE ( 'NONE', #12085, #8138, #18315, .T. ) ;
#19623=DIRECTION ( 'NONE',  ( 0.000000000000000000, -0.000000000000000000, 1.000000000000000000 ) ) ;
#19710=DIRECTION ( 'NONE',  ( 0.000000000000000000, 0.000000000000000000, -1.000000000000000000 ) ) ;
#19760=ADVANCED_FACE ( 'NONE', ( #20308 ), #2332, .T. ) ;
#19795=CARTESIAN_POINT ( 'NONE',  ( 0.000000000000000000, -14.99147757894464306, 6.724999999999999645 ) ) ;
#19799=CARTESIAN_POINT ( 'NONE',  ( -10.83999999999999986, -14.99147757894464306, 15.50000000000000000 ) ) ;
#19853=DIRECTION ( 'NONE',  ( 0.000000000000000000, 0.000000000000000000, 1.000000000000000000 ) ) ;
#19884=ORIENTED_EDGE ( 'NONE', *, *, #10366, .T. ) ;
#19985=DIRECTION ( 'NONE',  ( 0.000000000000000000, 0.000000000000000000, 1.000000000000000000 ) ) ;
#20091=CIRCLE ( 'NONE', #14239, 0.9999999999999991118 ) ;
#20104=VECTOR ( 'NONE', #20714, 1000.000000000000000 ) ;
#20110=ADVANCED_FACE ( 'NONE', ( #7195 ), #21969, .F. ) ;
#20121=DIRECTION ( 'NONE',  ( 0.000000000000000000, 0.000000000000000000, 1.000000000000000000 ) ) ;
#20123=DIRECTION ( 'NONE',  ( 0.000000000000000000, 0.000000000000000000, 1.000000000000000000 ) ) ;
#20178=EDGE_LOOP ( 'NONE', ( #15413, #2726, #17297, #15748 ) ) ;
#20188=ORIENTED_EDGE ( 'NONE', *, *, #20208, .T. ) ;
#20208=EDGE_CURVE ( 'NONE', #15969, #13092, #23410, .T. ) ;
#20213=AXIS2_PLACEMENT_3D ( 'NONE', #12953, #22373, #1868 ) ;
#20232=DIRECTION ( 'NONE',  ( -1.000000000000000000, 0.000000000000000000, 0.000000000000000000 ) ) ;
#20308=FACE_OUTER_BOUND ( 'NONE', #20178, .T. ) ;
#20367=PLANE ( 'NONE',  #13684 ) ;
#20403=DIRECTION ( 'NONE',  ( 1.000000000000000000, 0.000000000000000000, -0.000000000000000000 ) ) ;
#20432=CARTESIAN_POINT ( 'NONE',  ( -10.83999999999999986, -14.99147757894464306, 0.000000000000000000 ) ) ;
#20435=ORIENTED_EDGE ( 'NONE', *, *, #8564, .T. ) ;
#20495=DIRECTION ( 'NONE',  ( 1.000000000000000000, 0.000000000000000000, 0.000000000000000000 ) ) ;
#20519=ADVANCED_FACE ( 'NONE', ( #22073 ), #18391, .T. ) ;
#20583=ORIENTED_EDGE ( 'NONE', *, *, #10546, .T. ) ;
#20609=CARTESIAN_POINT ( 'NONE',  ( 1.255262969126036846E-16, -14.99147757894464306, 8.775000000000000355 ) ) ;
#20675=ORIENTED_EDGE ( 'NONE', *, *, #22969, .F. ) ;
#20683=ADVANCED_FACE ( 'NONE', ( #23536 ), #20836, .F. ) ;
#20714=DIRECTION ( 'NONE',  ( -0.000000000000000000, -0.000000000000000000, -1.000000000000000000 ) ) ;
#20749=LINE ( 'NONE', #147, #2397 ) ;
#20836=CONICAL_SURFACE ( 'NONE', #23949, 0.9999999999999991118, 1.029744258676654090 ) ;
#20847=AXIS2_PLACEMENT_3D ( 'NONE', #2955, #16239, #10494 ) ;
#20885=DIRECTION ( 'NONE',  ( -0.000000000000000000, -0.000000000000000000, -1.000000000000000000 ) ) ;
#21121=AXIS2_PLACEMENT_3D ( 'NONE', #22807, #22556, #17168 ) ;
#21153=EDGE_LOOP ( 'NONE', ( #6247, #4269, #20188, #771 ) ) ;
#21184=AXIS2_PLACEMENT_3D ( 'NONE', #390, #18691, #7797 ) ;
#21199=EDGE_CURVE ( 'NONE', #16945, #12085, #604, .T. ) ;
#21335=UNCERTAINTY_MEASURE_WITH_UNIT (LENGTH_MEASURE( 1.000000000000000082E-05 ), #15070, 'distance_accuracy_value', 'NONE');
#21433=AXIS2_PLACEMENT_3D ( 'NONE', #23160, #6445, #19623 ) ;
#21470=CARTESIAN_POINT ( 'NONE',  ( 0.000000000000000000, 0.000000000000000000, 15.50000000000000000 ) ) ;
#21472=ORIENTED_EDGE ( 'NONE', *, *, #10366, .F. ) ;
#21477=ORIENTED_EDGE ( 'NONE', *, *, #2367, .T. ) ;
#21484=APPLICATION_CONTEXT ( 'automotive_design' ) ;
#21539=CIRCLE ( 'NONE', #8662, 18.50000000000000000 ) ;
#21672=( GEOMETRIC_REPRESENTATION_CONTEXT ( 3 ) GLOBAL_UNCERTAINTY_ASSIGNED_CONTEXT ( ( #23296 ) ) GLOBAL_UNIT_ASSIGNED_CONTEXT ( ( #19, #13047, #15215 ) ) REPRESENTATION_CONTEXT ( 'NONE', 'WORKASPACE' ) );
#21791=CARTESIAN_POINT ( 'NONE',  ( 0.000000000000000000, 0.000000000000000000, 15.50000000000000000 ) ) ;
#21841=DIRECTION ( 'NONE',  ( 0.000000000000000000, 0.000000000000000000, 1.000000000000000000 ) ) ;
#21939=DIRECTION ( 'NONE',  ( -0.000000000000000000, -0.000000000000000000, -1.000000000000000000 ) ) ;
#21969=CYLINDRICAL_SURFACE ( 'NONE', #1577, 0.9999999999999991118 ) ;
#22073=FACE_OUTER_BOUND ( 'NONE', #7002, .T. ) ;
#22139=EDGE_CURVE ( 'NONE', #3902, #3687, #6484, .T. ) ;
#22344=DIRECTION ( 'NONE',  ( 0.000000000000000000, 0.000000000000000000, 1.000000000000000000 ) ) ;
#22373=DIRECTION ( 'NONE',  ( -0.000000000000000000, -1.000000000000000000, -0.000000000000000000 ) ) ;
#22399=DIRECTION ( 'NONE',  ( 1.000000000000000000, 0.000000000000000000, 0.000000000000000000 ) ) ;
#22423=DIRECTION ( 'NONE',  ( 1.000000000000000000, 0.000000000000000000, 0.000000000000000000 ) ) ;
#22555=CARTESIAN_POINT ( 'NONE',  ( 9.999999999999998224, 1.224646799147353059E-15, 0.000000000000000000 ) ) ;
#22556=DIRECTION ( 'NONE',  ( -0.000000000000000000, -1.000000000000000000, -0.000000000000000000 ) ) ;
#22807=CARTESIAN_POINT ( 'NONE',  ( 0.000000000000000000, -12.99147757894464306, 7.750000000000000000 ) ) ;
#22936=CARTESIAN_POINT ( 'NONE',  ( 0.000000000000000000, 0.000000000000000000, 15.50000000000000000 ) ) ;
#22960=DIRECTION ( 'NONE',  ( -0.000000000000000000, -0.000000000000000000, -1.000000000000000000 ) ) ;
#22969=EDGE_CURVE ( 'NONE', #3902, #4778, #4253, .T. ) ;
#23160=CARTESIAN_POINT ( 'NONE',  ( -10.83999999999999986, -14.99147757894464306, 15.50000000000000000 ) ) ;
#23276=CARTESIAN_POINT ( 'NONE',  ( -10.83999999999999986, -14.99147757894464306, 15.50000000000000000 ) ) ;
#23277=DIRECTION ( 'NONE',  ( -1.000000000000000000, 0.000000000000000000, 0.000000000000000000 ) ) ;
#23296=UNCERTAINTY_MEASURE_WITH_UNIT (LENGTH_MEASURE( 1.000000000000000082E-05 ), #19, 'distance_accuracy_value', 'NONE');
#23395=CONICAL_SURFACE ( 'NONE', #20213, 1.024999999999999911, 0.7853981633974396193 ) ;
#23410=CIRCLE ( 'NONE', #9709, 18.50000000000000000 ) ;
#23472=CARTESIAN_POINT ( 'NONE',  ( -9.999999999999998224, 0.000000000000000000, 15.50000000000000000 ) ) ;
#23491=VECTOR ( 'NONE', #17539, 1000.000000000000000 ) ;
#23512=CARTESIAN_POINT ( 'NONE',  ( 0.000000000000000000, 0.000000000000000000, 15.50000000000000000 ) ) ;
#23536=FACE_OUTER_BOUND ( 'NONE', #3749, .T. ) ;
#23659=CARTESIAN_POINT ( 'NONE',  ( 1.224646799147352468E-16, -12.99147757894464306, 8.749999999999998224 ) ) ;
#23677=FACE_OUTER_BOUND ( 'NONE', #14066, .T. ) ;
#23727=ORIENTED_EDGE ( 'NONE', *, *, #15188, .T. ) ;
#23749=CARTESIAN_POINT ( 'NONE',  ( 0.000000000000000000, -14.99147757894464306, 6.724999999999999645 ) ) ;
#23837=ORIENTED_EDGE ( 'NONE', *, *, #9142, .T. ) ;
#23841=AXIS2_PLACEMENT_3D ( 'NONE', #3832, #16523, #16648 ) ;
#23898=CARTESIAN_POINT ( 'NONE',  ( 0.000000000000000000, -14.99147757894464306, 7.750000000000000000 ) ) ;
#23949=AXIS2_PLACEMENT_3D ( 'NONE', #8513, #12155, #10083 ) ;
#24039=DIRECTION ( 'NONE',  ( -0.000000000000000000, -1.000000000000000000, -0.000000000000000000 ) ) ;
#24066=FACE_OUTER_BOUND ( 'NONE', #15141, .T. ) ;
#24071=ORIENTED_EDGE ( 'NONE', *, *, #16187, .F. ) ;
#24135=COLOUR_RGB('Light Blue',0.38,0.62,0.78);
#24136=FILL_AREA_STYLE_COLOUR('',#24135);
#24137=FILL_AREA_STYLE('',(#24136));
#24138=SURFACE_STYLE_FILL_AREA(#24137);
#24139=SURFACE_SIDE_STYLE('',(#24138));
#24140=SURFACE_STYLE_USAGE(.BOTH.,#24139);
#24141=PRESENTATION_STYLE_ASSIGNMENT((#24140));
ENDSEC;
END-ISO-10303-21;
